ISO-10303-21;
HEADER;
/* Generated by software containing ST-Developer
 * from STEP Tools, Inc. (www.steptools.com) 
 */

FILE_DESCRIPTION(
/* description */ ('Shaft runout checking stand'),
/* implementation_level */ '2;1');

FILE_NAME(
/* name */ 'Axle keeper (2).step',
/* time_stamp */ '2026-11-02T21:12:33-08:00',
/* author */ (''),
/* organization */ (''),
/* preprocessor_version */ 'ST-DEVELOPER v20.2',
/* originating_system */ 'Autodesk Translation Framework v15.17.0.0',
/* authorisation */ '');

FILE_SCHEMA (('AUTOMOTIVE_DESIGN { 1 0 10303 214 3 1 1 }'));
ENDSEC;

DATA;
#10=MECHANICAL_DESIGN_GEOMETRIC_PRESENTATION_REPRESENTATION('',(#481),#11748);
#395=SHAPE_REPRESENTATION_RELATIONSHIP('SRR','None',#11944,#438);
#438=ADVANCED_BREP_SHAPE_REPRESENTATION('',(#531),#11720);
#481=STYLED_ITEM('',(#12169),#531);
#531=MANIFOLD_SOLID_BREP('Body1',#6225);
#626=FACE_BOUND('',#1658,.T.);
#627=FACE_BOUND('',#1660,.T.);
#777=CIRCLE('',#7047,0.225);
#778=CIRCLE('',#7048,0.225);
#779=CIRCLE('',#7050,0.8);
#780=CIRCLE('',#7051,0.8);
#987=CYLINDRICAL_SURFACE('',#7046,0.225);
#988=CYLINDRICAL_SURFACE('',#7049,0.8);
#1223=FACE_OUTER_BOUND('',#1655,.T.);
#1224=FACE_OUTER_BOUND('',#1656,.T.);
#1225=FACE_OUTER_BOUND('',#1657,.T.);
#1226=FACE_OUTER_BOUND('',#1659,.T.);
#1655=EDGE_LOOP('',(#4926,#4927,#4928,#4929));
#1656=EDGE_LOOP('',(#4930,#4931,#4932,#4933));
#1657=EDGE_LOOP('',(#4934));
#1658=EDGE_LOOP('',(#4935));
#1659=EDGE_LOOP('',(#4936));
#1660=EDGE_LOOP('',(#4937));
#2198=LINE('',#10382,#2665);
#2199=LINE('',#10388,#2666);
#2665=VECTOR('',#8433,0.225);
#2666=VECTOR('',#8440,0.8);
#3097=VERTEX_POINT('',#10379);
#3098=VERTEX_POINT('',#10381);
#3099=VERTEX_POINT('',#10385);
#3100=VERTEX_POINT('',#10387);
#3749=EDGE_CURVE('',#3097,#3097,#777,.T.);
#3750=EDGE_CURVE('',#3097,#3098,#2198,.T.);
#3751=EDGE_CURVE('',#3098,#3098,#778,.T.);
#3752=EDGE_CURVE('',#3099,#3099,#779,.T.);
#3753=EDGE_CURVE('',#3099,#3100,#2199,.T.);
#3754=EDGE_CURVE('',#3100,#3100,#780,.T.);
#4926=ORIENTED_EDGE('',*,*,#3749,.F.);
#4927=ORIENTED_EDGE('',*,*,#3750,.T.);
#4928=ORIENTED_EDGE('',*,*,#3751,.T.);
#4929=ORIENTED_EDGE('',*,*,#3750,.F.);
#4930=ORIENTED_EDGE('',*,*,#3752,.F.);
#4931=ORIENTED_EDGE('',*,*,#3753,.T.);
#4932=ORIENTED_EDGE('',*,*,#3754,.T.);
#4933=ORIENTED_EDGE('',*,*,#3753,.F.);
#4934=ORIENTED_EDGE('',*,*,#3752,.T.);
#4935=ORIENTED_EDGE('',*,*,#3749,.T.);
#4936=ORIENTED_EDGE('',*,*,#3754,.F.);
#4937=ORIENTED_EDGE('',*,*,#3751,.F.);
#5736=PLANE('',#7052);
#5737=PLANE('',#7053);
#6023=ADVANCED_FACE('',(#1223),#987,.F.);
#6024=ADVANCED_FACE('',(#1224),#988,.T.);
#6025=ADVANCED_FACE('',(#1225,#626),#5736,.T.);
#6026=ADVANCED_FACE('',(#1226,#627),#5737,.F.);
#6225=CLOSED_SHELL('',(#6023,#6024,#6025,#6026));
#7045=AXIS2_PLACEMENT_3D('',#10377,#8427,#8428);
#7046=AXIS2_PLACEMENT_3D('',#10378,#8429,#8430);
#7047=AXIS2_PLACEMENT_3D('',#10380,#8431,#8432);
#7048=AXIS2_PLACEMENT_3D('',#10383,#8434,#8435);
#7049=AXIS2_PLACEMENT_3D('',#10384,#8436,#8437);
#7050=AXIS2_PLACEMENT_3D('',#10386,#8438,#8439);
#7051=AXIS2_PLACEMENT_3D('',#10389,#8441,#8442);
#7052=AXIS2_PLACEMENT_3D('',#10390,#8443,#8444);
#7053=AXIS2_PLACEMENT_3D('',#10391,#8445,#8446);
#8427=DIRECTION('axis',(0.,0.,1.));
#8428=DIRECTION('refdir',(1.,0.,0.));
#8429=DIRECTION('center_axis',(0.,1.,0.));
#8430=DIRECTION('ref_axis',(1.,0.,0.));
#8431=DIRECTION('center_axis',(0.,-1.,0.));
#8432=DIRECTION('ref_axis',(1.,0.,0.));
#8433=DIRECTION('',(0.,-1.,0.));
#8434=DIRECTION('center_axis',(0.,-1.,0.));
#8435=DIRECTION('ref_axis',(1.,0.,0.));
#8436=DIRECTION('center_axis',(0.,1.,0.));
#8437=DIRECTION('ref_axis',(1.,0.,0.));
#8438=DIRECTION('center_axis',(0.,1.,0.));
#8439=DIRECTION('ref_axis',(1.,0.,0.));
#8440=DIRECTION('',(0.,-1.,0.));
#8441=DIRECTION('center_axis',(0.,1.,0.));
#8442=DIRECTION('ref_axis',(1.,0.,0.));
#8443=DIRECTION('center_axis',(0.,1.,0.));
#8444=DIRECTION('ref_axis',(1.,0.,0.));
#8445=DIRECTION('center_axis',(0.,1.,0.));
#8446=DIRECTION('ref_axis',(1.,0.,0.));
#10377=CARTESIAN_POINT('',(0.,0.,0.));
#10378=CARTESIAN_POINT('Origin',(-2.,10.8,5.));
#10379=CARTESIAN_POINT('',(-2.225,11.,5.));
#10380=CARTESIAN_POINT('Origin',(-2.,11.,5.));
#10381=CARTESIAN_POINT('',(-2.225,10.8,5.));
#10382=CARTESIAN_POINT('',(-2.225,10.8,5.));
#10383=CARTESIAN_POINT('Origin',(-2.,10.8,5.));
#10384=CARTESIAN_POINT('Origin',(-2.,10.8,5.));
#10385=CARTESIAN_POINT('',(-2.8,11.,5.));
#10386=CARTESIAN_POINT('Origin',(-2.,11.,5.));
#10387=CARTESIAN_POINT('',(-2.8,10.8,5.));
#10388=CARTESIAN_POINT('',(-2.8,10.8,5.));
#10389=CARTESIAN_POINT('Origin',(-2.,10.8,5.));
#10390=CARTESIAN_POINT('Origin',(-2.,11.,5.));
#10391=CARTESIAN_POINT('Origin',(-2.,10.8,5.));
#11671=UNCERTAINTY_MEASURE_WITH_UNIT(LENGTH_MEASURE(0.001),#11749,
'DISTANCE_ACCURACY_VALUE',
'Maximum model space distance between geometric entities at asserted c
onnectivities');
#11699=UNCERTAINTY_MEASURE_WITH_UNIT(LENGTH_MEASURE(0.001),#11749,
'DISTANCE_ACCURACY_VALUE',
'Maximum model space distance between geometric entities at asserted c
onnectivities');
#11720=(
GEOMETRIC_REPRESENTATION_CONTEXT(3)
GLOBAL_UNCERTAINTY_ASSIGNED_CONTEXT((#11671))
GLOBAL_UNIT_ASSIGNED_CONTEXT((#11749,#11751,#11752))
REPRESENTATION_CONTEXT('','3D')
);
#11748=(
GEOMETRIC_REPRESENTATION_CONTEXT(3)
GLOBAL_UNCERTAINTY_ASSIGNED_CONTEXT((#11699))
GLOBAL_UNIT_ASSIGNED_CONTEXT((#11749,#11751,#11752))
REPRESENTATION_CONTEXT('','3D')
);
#11749=(
LENGTH_UNIT()
NAMED_UNIT(*)
SI_UNIT(.CENTI.,.METRE.)
);
#11751=(
NAMED_UNIT(*)
PLANE_ANGLE_UNIT()
SI_UNIT($,.RADIAN.)
);
#11752=(
NAMED_UNIT(*)
SI_UNIT($,.STERADIAN.)
SOLID_ANGLE_UNIT()
);
#11773=SHAPE_DEFINITION_REPRESENTATION(#11821,#11944);
#11821=PRODUCT_DEFINITION_SHAPE('',$,#11993);
#11944=SHAPE_REPRESENTATION('',(#7045),#11720);
#11972=PRODUCT_DEFINITION_CONTEXT('part definition',#12118,'design');
#11993=PRODUCT_DEFINITION('Axle keeper_2','Axle keeper (2)',#12041,#11972);
#12041=PRODUCT_DEFINITION_FORMATION('',$,#12140);
#12118=APPLICATION_CONTEXT(
'Core Data for Automotive Mechanical Design Process');
#12119=PRODUCT_CONTEXT('part definition',#12118,'mechanical');
#12140=PRODUCT('Axle keeper_2','Axle keeper (2)','Axle keeper',(#12119));
#12169=PRESENTATION_STYLE_ASSIGNMENT((#12174));
#12174=SURFACE_STYLE_USAGE(.BOTH.,#12179);
#12179=SURFACE_SIDE_STYLE('',(#12184));
#12184=SURFACE_STYLE_FILL_AREA(#12189);
#12189=FILL_AREA_STYLE('CAD Library Painted - Engineering blue',(#12194));
#12194=FILL_AREA_STYLE_COLOUR('CAD Library Painted - Engineering blue',
#12199);
#12199=COLOUR_RGB('CAD Library Painted - Engineering blue',0.12156862745098,
0.356862745098039,0.6);
ENDSEC;
END-ISO-10303-21;
